ISO-10303-21;
HEADER;
/* Generated by software containing ST-Developer
 * from STEP Tools, Inc. (www.steptools.com) 
 */

FILE_DESCRIPTION(
/* description */ ('XY cross-slide table'),
/* implementation_level */ '2;1');

FILE_NAME(
/* name */ 'Cap Screw - M6x25.step',
/* time_stamp */ '2026-10-28T03:22:46-07:00',
/* author */ (''),
/* organization */ (''),
/* preprocessor_version */ 'ST-DEVELOPER v20.2',
/* originating_system */ 'Autodesk Translation Framework v15.17.0.0',
/* authorisation */ '');

FILE_SCHEMA (('AUTOMOTIVE_DESIGN { 1 0 10303 214 3 1 1 }'));
ENDSEC;

DATA;
#10=MECHANICAL_DESIGN_GEOMETRIC_PRESENTATION_REPRESENTATION('',(#1726),#62984);
#22=ORIENTED_CLOSED_SHELL('',*,#23024,.F.);
#31=BREP_WITH_VOIDS('Body1',#23023,(#22));
#1463=CONICAL_SURFACE('',#25130,0.475,0.785398163397449);
#1464=CONICAL_SURFACE('',#25134,0.485,0.785398163397448);
#1465=CONICAL_SURFACE('',#25138,0.31,0.463647609000806);
#1466=CONICAL_SURFACE('',#25142,0.27,0.785398163397448);
#1545=SHAPE_REPRESENTATION_RELATIONSHIP('SRR','None',#63398,#1628);
#1628=ADVANCED_BREP_SHAPE_REPRESENTATION('',(#31),#62935);
#1726=STYLED_ITEM('',(#63919),#31);
#2084=FACE_BOUND('',#5011,.T.);
#2566=PLANE('',#25128);
#2567=PLANE('',#25136);
#2568=PLANE('',#25144);
#2569=PLANE('',#25145);
#2570=PLANE('',#25146);
#2571=PLANE('',#25147);
#2572=PLANE('',#25148);
#2573=PLANE('',#25149);
#2574=PLANE('',#25150);
#2575=PLANE('',#25151);
#2576=PLANE('',#25152);
#3495=FACE_OUTER_BOUND('',#5006,.T.);
#3496=FACE_OUTER_BOUND('',#5007,.T.);
#3497=FACE_OUTER_BOUND('',#5008,.T.);
#3498=FACE_OUTER_BOUND('',#5009,.T.);
#3499=FACE_OUTER_BOUND('',#5010,.T.);
#3500=FACE_OUTER_BOUND('',#5012,.T.);
#3501=FACE_OUTER_BOUND('',#5013,.T.);
#3502=FACE_OUTER_BOUND('',#5014,.T.);
#3503=FACE_OUTER_BOUND('',#5015,.T.);
#3504=FACE_OUTER_BOUND('',#5016,.T.);
#3505=FACE_OUTER_BOUND('',#5017,.T.);
#3506=FACE_OUTER_BOUND('',#5018,.T.);
#3507=FACE_OUTER_BOUND('',#5019,.T.);
#3508=FACE_OUTER_BOUND('',#5020,.T.);
#3509=FACE_OUTER_BOUND('',#5021,.T.);
#3510=FACE_OUTER_BOUND('',#5022,.T.);
#3511=FACE_OUTER_BOUND('',#5023,.T.);
#5006=EDGE_LOOP('',(#17866));
#5007=EDGE_LOOP('',(#17867,#17868,#17869,#17870));
#5008=EDGE_LOOP('',(#17871,#17872,#17873,#17874));
#5009=EDGE_LOOP('',(#17875,#17876,#17877,#17878));
#5010=EDGE_LOOP('',(#17879));
#5011=EDGE_LOOP('',(#17880));
#5012=EDGE_LOOP('',(#17881,#17882,#17883,#17884));
#5013=EDGE_LOOP('',(#17885,#17886,#17887,#17888));
#5014=EDGE_LOOP('',(#17889,#17890,#17891,#17892));
#5015=EDGE_LOOP('',(#17893));
#5016=EDGE_LOOP('',(#17894,#17895,#17896,#17897));
#5017=EDGE_LOOP('',(#17898,#17899,#17900,#17901));
#5018=EDGE_LOOP('',(#17902,#17903,#17904,#17905));
#5019=EDGE_LOOP('',(#17906,#17907,#17908,#17909));
#5020=EDGE_LOOP('',(#17910,#17911,#17912,#17913));
#5021=EDGE_LOOP('',(#17914,#17915,#17916,#17917));
#5022=EDGE_LOOP('',(#17918,#17919,#17920,#17921,#17922,#17923));
#5023=EDGE_LOOP('',(#17924,#17925,#17926,#17927,#17928,#17929));
#6620=LINE('',#47669,#8107);
#6621=LINE('',#47673,#8108);
#6622=LINE('',#47677,#8109);
#6623=LINE('',#47684,#8110);
#6624=LINE('',#47688,#8111);
#6625=LINE('',#47692,#8112);
#6626=LINE('',#47697,#8113);
#6627=LINE('',#47699,#8114);
#6628=LINE('',#47701,#8115);
#6629=LINE('',#47702,#8116);
#6630=LINE('',#47705,#8117);
#6631=LINE('',#47707,#8118);
#6632=LINE('',#47708,#8119);
#6633=LINE('',#47711,#8120);
#6634=LINE('',#47713,#8121);
#6635=LINE('',#47714,#8122);
#6636=LINE('',#47717,#8123);
#6637=LINE('',#47719,#8124);
#6638=LINE('',#47720,#8125);
#6639=LINE('',#47723,#8126);
#6640=LINE('',#47725,#8127);
#6641=LINE('',#47726,#8128);
#6642=LINE('',#47728,#8129);
#6643=LINE('',#47729,#8130);
#8107=VECTOR('',#29439,0.475);
#8108=VECTOR('',#29444,0.5);
#8109=VECTOR('',#29449,0.485);
#8110=VECTOR('',#29458,0.31);
#8111=VECTOR('',#29463,0.3);
#8112=VECTOR('',#29468,0.27);
#8113=VECTOR('',#29473,1.);
#8114=VECTOR('',#29474,1.);
#8115=VECTOR('',#29475,1.);
#8116=VECTOR('',#29476,1.);
#8117=VECTOR('',#29479,1.);
#8118=VECTOR('',#29480,1.);
#8119=VECTOR('',#29481,1.);
#8120=VECTOR('',#29484,1.);
#8121=VECTOR('',#29485,1.);
#8122=VECTOR('',#29486,1.);
#8123=VECTOR('',#29489,1.);
#8124=VECTOR('',#29490,1.);
#8125=VECTOR('',#29491,1.);
#8126=VECTOR('',#29494,1.);
#8127=VECTOR('',#29495,1.);
#8128=VECTOR('',#29496,1.);
#8129=VECTOR('',#29499,1.);
#8130=VECTOR('',#29500,1.);
#9303=CIRCLE('',#25129,0.45);
#9304=CIRCLE('',#25131,0.5);
#9305=CIRCLE('',#25133,0.5);
#9306=CIRCLE('',#25135,0.47);
#9307=CIRCLE('',#25137,0.32);
#9308=CIRCLE('',#25139,0.2942);
#9309=CIRCLE('',#25141,0.2942);
#9310=CIRCLE('',#25143,0.24);
#10771=VERTEX_POINT('',#47664);
#10772=VERTEX_POINT('',#47667);
#10773=VERTEX_POINT('',#47671);
#10774=VERTEX_POINT('',#47675);
#10775=VERTEX_POINT('',#47679);
#10776=VERTEX_POINT('',#47682);
#10777=VERTEX_POINT('',#47686);
#10778=VERTEX_POINT('',#47690);
#10779=VERTEX_POINT('',#47695);
#10780=VERTEX_POINT('',#47696);
#10781=VERTEX_POINT('',#47698);
#10782=VERTEX_POINT('',#47700);
#10783=VERTEX_POINT('',#47704);
#10784=VERTEX_POINT('',#47706);
#10785=VERTEX_POINT('',#47710);
#10786=VERTEX_POINT('',#47712);
#10787=VERTEX_POINT('',#47716);
#10788=VERTEX_POINT('',#47718);
#10789=VERTEX_POINT('',#47722);
#10790=VERTEX_POINT('',#47724);
#13317=EDGE_CURVE('',#10771,#10771,#9303,.T.);
#13318=EDGE_CURVE('',#10772,#10772,#9304,.T.);
#13319=EDGE_CURVE('',#10772,#10771,#6620,.T.);
#13320=EDGE_CURVE('',#10773,#10773,#9305,.T.);
#13321=EDGE_CURVE('',#10773,#10772,#6621,.T.);
#13322=EDGE_CURVE('',#10774,#10774,#9306,.T.);
#13323=EDGE_CURVE('',#10774,#10773,#6622,.T.);
#13324=EDGE_CURVE('',#10775,#10775,#9307,.T.);
#13325=EDGE_CURVE('',#10776,#10776,#9308,.F.);
#13326=EDGE_CURVE('',#10776,#10775,#6623,.T.);
#13327=EDGE_CURVE('',#10777,#10777,#9309,.F.);
#13328=EDGE_CURVE('',#10777,#10776,#6624,.T.);
#13329=EDGE_CURVE('',#10778,#10778,#9310,.T.);
#13330=EDGE_CURVE('',#10778,#10777,#6625,.T.);
#13331=EDGE_CURVE('',#10779,#10780,#6626,.T.);
#13332=EDGE_CURVE('',#10780,#10781,#6627,.T.);
#13333=EDGE_CURVE('',#10781,#10782,#6628,.T.);
#13334=EDGE_CURVE('',#10779,#10782,#6629,.T.);
#13335=EDGE_CURVE('',#10780,#10783,#6630,.T.);
#13336=EDGE_CURVE('',#10783,#10784,#6631,.T.);
#13337=EDGE_CURVE('',#10784,#10781,#6632,.T.);
#13338=EDGE_CURVE('',#10783,#10785,#6633,.T.);
#13339=EDGE_CURVE('',#10785,#10786,#6634,.T.);
#13340=EDGE_CURVE('',#10786,#10784,#6635,.T.);
#13341=EDGE_CURVE('',#10785,#10787,#6636,.T.);
#13342=EDGE_CURVE('',#10787,#10788,#6637,.T.);
#13343=EDGE_CURVE('',#10788,#10786,#6638,.T.);
#13344=EDGE_CURVE('',#10787,#10789,#6639,.T.);
#13345=EDGE_CURVE('',#10789,#10790,#6640,.T.);
#13346=EDGE_CURVE('',#10790,#10788,#6641,.T.);
#13347=EDGE_CURVE('',#10789,#10779,#6642,.T.);
#13348=EDGE_CURVE('',#10782,#10790,#6643,.T.);
#17866=ORIENTED_EDGE('',*,*,#13317,.F.);
#17867=ORIENTED_EDGE('',*,*,#13318,.F.);
#17868=ORIENTED_EDGE('',*,*,#13319,.T.);
#17869=ORIENTED_EDGE('',*,*,#13317,.T.);
#17870=ORIENTED_EDGE('',*,*,#13319,.F.);
#17871=ORIENTED_EDGE('',*,*,#13320,.F.);
#17872=ORIENTED_EDGE('',*,*,#13321,.T.);
#17873=ORIENTED_EDGE('',*,*,#13318,.T.);
#17874=ORIENTED_EDGE('',*,*,#13321,.F.);
#17875=ORIENTED_EDGE('',*,*,#13322,.F.);
#17876=ORIENTED_EDGE('',*,*,#13323,.T.);
#17877=ORIENTED_EDGE('',*,*,#13320,.T.);
#17878=ORIENTED_EDGE('',*,*,#13323,.F.);
#17879=ORIENTED_EDGE('',*,*,#13322,.T.);
#17880=ORIENTED_EDGE('',*,*,#13324,.F.);
#17881=ORIENTED_EDGE('',*,*,#13325,.F.);
#17882=ORIENTED_EDGE('',*,*,#13326,.T.);
#17883=ORIENTED_EDGE('',*,*,#13324,.T.);
#17884=ORIENTED_EDGE('',*,*,#13326,.F.);
#17885=ORIENTED_EDGE('',*,*,#13327,.F.);
#17886=ORIENTED_EDGE('',*,*,#13328,.T.);
#17887=ORIENTED_EDGE('',*,*,#13325,.T.);
#17888=ORIENTED_EDGE('',*,*,#13328,.F.);
#17889=ORIENTED_EDGE('',*,*,#13329,.F.);
#17890=ORIENTED_EDGE('',*,*,#13330,.T.);
#17891=ORIENTED_EDGE('',*,*,#13327,.T.);
#17892=ORIENTED_EDGE('',*,*,#13330,.F.);
#17893=ORIENTED_EDGE('',*,*,#13329,.T.);
#17894=ORIENTED_EDGE('',*,*,#13331,.T.);
#17895=ORIENTED_EDGE('',*,*,#13332,.T.);
#17896=ORIENTED_EDGE('',*,*,#13333,.T.);
#17897=ORIENTED_EDGE('',*,*,#13334,.F.);
#17898=ORIENTED_EDGE('',*,*,#13335,.T.);
#17899=ORIENTED_EDGE('',*,*,#13336,.T.);
#17900=ORIENTED_EDGE('',*,*,#13337,.T.);
#17901=ORIENTED_EDGE('',*,*,#13332,.F.);
#17902=ORIENTED_EDGE('',*,*,#13338,.T.);
#17903=ORIENTED_EDGE('',*,*,#13339,.T.);
#17904=ORIENTED_EDGE('',*,*,#13340,.T.);
#17905=ORIENTED_EDGE('',*,*,#13336,.F.);
#17906=ORIENTED_EDGE('',*,*,#13341,.T.);
#17907=ORIENTED_EDGE('',*,*,#13342,.T.);
#17908=ORIENTED_EDGE('',*,*,#13343,.T.);
#17909=ORIENTED_EDGE('',*,*,#13339,.F.);
#17910=ORIENTED_EDGE('',*,*,#13344,.T.);
#17911=ORIENTED_EDGE('',*,*,#13345,.T.);
#17912=ORIENTED_EDGE('',*,*,#13346,.T.);
#17913=ORIENTED_EDGE('',*,*,#13342,.F.);
#17914=ORIENTED_EDGE('',*,*,#13347,.T.);
#17915=ORIENTED_EDGE('',*,*,#13334,.T.);
#17916=ORIENTED_EDGE('',*,*,#13348,.T.);
#17917=ORIENTED_EDGE('',*,*,#13345,.F.);
#17918=ORIENTED_EDGE('',*,*,#13347,.F.);
#17919=ORIENTED_EDGE('',*,*,#13344,.F.);
#17920=ORIENTED_EDGE('',*,*,#13341,.F.);
#17921=ORIENTED_EDGE('',*,*,#13338,.F.);
#17922=ORIENTED_EDGE('',*,*,#13335,.F.);
#17923=ORIENTED_EDGE('',*,*,#13331,.F.);
#17924=ORIENTED_EDGE('',*,*,#13348,.F.);
#17925=ORIENTED_EDGE('',*,*,#13333,.F.);
#17926=ORIENTED_EDGE('',*,*,#13337,.F.);
#17927=ORIENTED_EDGE('',*,*,#13340,.F.);
#17928=ORIENTED_EDGE('',*,*,#13343,.F.);
#17929=ORIENTED_EDGE('',*,*,#13346,.F.);
#21336=CYLINDRICAL_SURFACE('',#25132,0.5);
#21337=CYLINDRICAL_SURFACE('',#25140,0.2942);
#22276=ADVANCED_FACE('',(#3495),#2566,.T.);
#22277=ADVANCED_FACE('',(#3496),#1463,.T.);
#22278=ADVANCED_FACE('',(#3497),#21336,.T.);
#22279=ADVANCED_FACE('',(#3498),#1464,.T.);
#22280=ADVANCED_FACE('',(#3499,#2084),#2567,.T.);
#22281=ADVANCED_FACE('',(#3500),#1465,.T.);
#22282=ADVANCED_FACE('',(#3501),#21337,.T.);
#22283=ADVANCED_FACE('',(#3502),#1466,.T.);
#22284=ADVANCED_FACE('',(#3503),#2568,.T.);
#22285=ADVANCED_FACE('',(#3504),#2569,.F.);
#22286=ADVANCED_FACE('',(#3505),#2570,.F.);
#22287=ADVANCED_FACE('',(#3506),#2571,.F.);
#22288=ADVANCED_FACE('',(#3507),#2572,.F.);
#22289=ADVANCED_FACE('',(#3508),#2573,.F.);
#22290=ADVANCED_FACE('',(#3509),#2574,.F.);
#22291=ADVANCED_FACE('',(#3510),#2575,.F.);
#22292=ADVANCED_FACE('',(#3511),#2576,.F.);
#23023=CLOSED_SHELL('',(#22276,#22277,#22278,#22279,#22280,#22281,#22282,
#22283,#22284));
#23024=CLOSED_SHELL('',(#22285,#22286,#22287,#22288,#22289,#22290,#22291,
#22292));
#25127=AXIS2_PLACEMENT_3D('',#47662,#29429,#29430);
#25128=AXIS2_PLACEMENT_3D('',#47663,#29431,#29432);
#25129=AXIS2_PLACEMENT_3D('',#47665,#29433,#29434);
#25130=AXIS2_PLACEMENT_3D('',#47666,#29435,#29436);
#25131=AXIS2_PLACEMENT_3D('',#47668,#29437,#29438);
#25132=AXIS2_PLACEMENT_3D('',#47670,#29440,#29441);
#25133=AXIS2_PLACEMENT_3D('',#47672,#29442,#29443);
#25134=AXIS2_PLACEMENT_3D('',#47674,#29445,#29446);
#25135=AXIS2_PLACEMENT_3D('',#47676,#29447,#29448);
#25136=AXIS2_PLACEMENT_3D('',#47678,#29450,#29451);
#25137=AXIS2_PLACEMENT_3D('',#47680,#29452,#29453);
#25138=AXIS2_PLACEMENT_3D('',#47681,#29454,#29455);
#25139=AXIS2_PLACEMENT_3D('',#47683,#29456,#29457);
#25140=AXIS2_PLACEMENT_3D('',#47685,#29459,#29460);
#25141=AXIS2_PLACEMENT_3D('',#47687,#29461,#29462);
#25142=AXIS2_PLACEMENT_3D('',#47689,#29464,#29465);
#25143=AXIS2_PLACEMENT_3D('',#47691,#29466,#29467);
#25144=AXIS2_PLACEMENT_3D('',#47693,#29469,#29470);
#25145=AXIS2_PLACEMENT_3D('',#47694,#29471,#29472);
#25146=AXIS2_PLACEMENT_3D('',#47703,#29477,#29478);
#25147=AXIS2_PLACEMENT_3D('',#47709,#29482,#29483);
#25148=AXIS2_PLACEMENT_3D('',#47715,#29487,#29488);
#25149=AXIS2_PLACEMENT_3D('',#47721,#29492,#29493);
#25150=AXIS2_PLACEMENT_3D('',#47727,#29497,#29498);
#25151=AXIS2_PLACEMENT_3D('',#47730,#29501,#29502);
#25152=AXIS2_PLACEMENT_3D('',#47731,#29503,#29504);
#29429=DIRECTION('axis',(0.,0.,1.));
#29430=DIRECTION('refdir',(1.,0.,0.));
#29431=DIRECTION('center_axis',(0.,1.,0.));
#29432=DIRECTION('ref_axis',(0.,0.,1.));
#29433=DIRECTION('center_axis',(0.,-1.,0.));
#29434=DIRECTION('ref_axis',(1.,0.,0.));
#29435=DIRECTION('center_axis',(0.,-1.,0.));
#29436=DIRECTION('ref_axis',(1.,0.,0.));
#29437=DIRECTION('center_axis',(0.,-1.,0.));
#29438=DIRECTION('ref_axis',(1.,0.,0.));
#29439=DIRECTION('',(0.707106781186548,0.707106781186547,8.65956056235494E-17));
#29440=DIRECTION('center_axis',(0.,-1.,0.));
#29441=DIRECTION('ref_axis',(1.,0.,0.));
#29442=DIRECTION('center_axis',(0.,-1.,0.));
#29443=DIRECTION('ref_axis',(1.,0.,0.));
#29444=DIRECTION('',(0.,1.,0.));
#29445=DIRECTION('center_axis',(0.,1.,0.));
#29446=DIRECTION('ref_axis',(1.,0.,0.));
#29447=DIRECTION('center_axis',(0.,-1.,0.));
#29448=DIRECTION('ref_axis',(1.,0.,0.));
#29449=DIRECTION('',(-0.707106781186547,0.707106781186548,-8.65956056235493E-17));
#29450=DIRECTION('center_axis',(0.,-1.,0.));
#29451=DIRECTION('ref_axis',(0.,0.,-1.));
#29452=DIRECTION('center_axis',(0.,-1.,0.));
#29453=DIRECTION('ref_axis',(1.,0.,0.));
#29454=DIRECTION('center_axis',(0.,1.,0.));
#29455=DIRECTION('ref_axis',(1.,0.,0.));
#29456=DIRECTION('center_axis',(0.,1.,0.));
#29457=DIRECTION('ref_axis',(1.,0.,0.));
#29458=DIRECTION('',(-0.447213595499958,0.894427190999916,-5.47678698264203E-17));
#29459=DIRECTION('center_axis',(0.,-1.,0.));
#29460=DIRECTION('ref_axis',(1.,0.,0.));
#29461=DIRECTION('center_axis',(0.,1.,0.));
#29462=DIRECTION('ref_axis',(1.,0.,0.));
#29463=DIRECTION('',(0.,1.,0.));
#29464=DIRECTION('center_axis',(0.,1.,0.));
#29465=DIRECTION('ref_axis',(1.,0.,0.));
#29466=DIRECTION('center_axis',(0.,-1.,0.));
#29467=DIRECTION('ref_axis',(1.,0.,0.));
#29468=DIRECTION('',(-0.707106781186547,0.707106781186548,-8.65956056235493E-17));
#29469=DIRECTION('center_axis',(0.,-1.,0.));
#29470=DIRECTION('ref_axis',(0.,0.,-1.));
#29471=DIRECTION('center_axis',(0.866025403784439,0.,-0.5));
#29472=DIRECTION('ref_axis',(0.5,0.,0.866025403784439));
#29473=DIRECTION('',(-0.5,0.,-0.866025403784439));
#29474=DIRECTION('',(0.,-1.,0.));
#29475=DIRECTION('',(0.5,0.,0.866025403784439));
#29476=DIRECTION('',(0.,-1.,0.));
#29477=DIRECTION('center_axis',(1.92296268638356E-16,0.,-1.));
#29478=DIRECTION('ref_axis',(1.,0.,1.92296268638356E-16));
#29479=DIRECTION('',(-1.,0.,-1.92296268638356E-16));
#29480=DIRECTION('',(0.,-1.,0.));
#29481=DIRECTION('',(1.,0.,1.92296268638356E-16));
#29482=DIRECTION('center_axis',(-0.866025403784439,0.,-0.5));
#29483=DIRECTION('ref_axis',(0.5,0.,-0.866025403784439));
#29484=DIRECTION('',(-0.5,0.,0.866025403784438));
#29485=DIRECTION('',(0.,-1.,0.));
#29486=DIRECTION('',(0.5,0.,-0.866025403784438));
#29487=DIRECTION('center_axis',(-0.866025403784439,0.,0.5));
#29488=DIRECTION('ref_axis',(-0.5,0.,-0.866025403784439));
#29489=DIRECTION('',(0.5,0.,0.866025403784439));
#29490=DIRECTION('',(0.,-1.,0.));
#29491=DIRECTION('',(-0.5,0.,-0.866025403784439));
#29492=DIRECTION('center_axis',(-1.92296268638356E-16,0.,1.));
#29493=DIRECTION('ref_axis',(-1.,0.,-1.92296268638356E-16));
#29494=DIRECTION('',(1.,0.,1.92296268638356E-16));
#29495=DIRECTION('',(0.,-1.,0.));
#29496=DIRECTION('',(-1.,0.,-1.92296268638356E-16));
#29497=DIRECTION('center_axis',(0.866025403784439,0.,0.5));
#29498=DIRECTION('ref_axis',(-0.5,0.,0.866025403784439));
#29499=DIRECTION('',(0.5,0.,-0.866025403784439));
#29500=DIRECTION('',(-0.5,0.,0.866025403784439));
#29501=DIRECTION('center_axis',(0.,1.,0.));
#29502=DIRECTION('ref_axis',(1.,0.,0.));
#29503=DIRECTION('center_axis',(0.,-1.,0.));
#29504=DIRECTION('ref_axis',(0.,0.,-1.));
#47662=CARTESIAN_POINT('',(0.,0.,0.));
#47663=CARTESIAN_POINT('Origin',(0.45,0.6,0.));
#47664=CARTESIAN_POINT('',(-0.45,0.6,-5.51091059616309E-17));
#47665=CARTESIAN_POINT('Origin',(0.,0.6,0.));
#47666=CARTESIAN_POINT('Origin',(0.,0.575,0.));
#47667=CARTESIAN_POINT('',(-0.5,0.55,-6.12323399573677E-17));
#47668=CARTESIAN_POINT('Origin',(0.,0.55,0.));
#47669=CARTESIAN_POINT('',(-0.475,0.575,-5.81707229594993E-17));
#47670=CARTESIAN_POINT('Origin',(0.,0.29,0.));
#47671=CARTESIAN_POINT('',(-0.5,0.0299999999999998,-6.12323399573677E-17));
#47672=CARTESIAN_POINT('Origin',(0.,0.0299999999999998,0.));
#47673=CARTESIAN_POINT('',(-0.5,0.29,-6.12323399573677E-17));
#47674=CARTESIAN_POINT('Origin',(0.,0.0150000000000001,0.));
#47675=CARTESIAN_POINT('',(-0.47,7.11236625150491E-17,-5.75583995599256E-17));
#47676=CARTESIAN_POINT('Origin',(0.,0.,0.));
#47677=CARTESIAN_POINT('',(-0.485,0.0150000000000001,-5.93953697586466E-17));
#47678=CARTESIAN_POINT('Origin',(0.32,0.,0.));
#47679=CARTESIAN_POINT('',(-0.32,-6.93889390390723E-18,-3.91886975727153E-17));
#47680=CARTESIAN_POINT('Origin',(0.,0.,0.));
#47681=CARTESIAN_POINT('Origin',(0.,-0.02,0.));
#47682=CARTESIAN_POINT('',(-0.2942,-0.0515999999999999,3.60291088309151E-17));
#47683=CARTESIAN_POINT('Origin',(0.,-0.0515999999999999,0.));
#47684=CARTESIAN_POINT('',(-0.31,-0.02,-3.7964050773568E-17));
#47685=CARTESIAN_POINT('Origin',(0.,-1.24,0.));
#47686=CARTESIAN_POINT('',(-0.2942,-2.4458,3.60291088309151E-17));
#47687=CARTESIAN_POINT('Origin',(0.,-2.4458,0.));
#47688=CARTESIAN_POINT('',(-0.2942,-1.24,-3.60291088309151E-17));
#47689=CARTESIAN_POINT('Origin',(0.,-2.47,0.));
#47690=CARTESIAN_POINT('',(-0.24,-2.5,-2.93915231795365E-17));
#47691=CARTESIAN_POINT('Origin',(0.,-2.5,0.));
#47692=CARTESIAN_POINT('',(-0.27,-2.47,-3.30654635769785E-17));
#47693=CARTESIAN_POINT('Origin',(0.,-2.5,0.));
#47694=CARTESIAN_POINT('Origin',(0.144337567297406,-0.6,-0.25));
#47695=CARTESIAN_POINT('',(0.288675134594813,-0.6,0.));
#47696=CARTESIAN_POINT('',(0.144337567297406,-0.6,-0.25));
#47697=CARTESIAN_POINT('',(0.288675134594813,-0.6,0.));
#47698=CARTESIAN_POINT('',(0.144337567297406,-0.96,-0.25));
#47699=CARTESIAN_POINT('',(0.144337567297406,-0.6,-0.25));
#47700=CARTESIAN_POINT('',(0.288675134594813,-0.96,0.));
#47701=CARTESIAN_POINT('',(0.288675134594813,-0.96,0.));
#47702=CARTESIAN_POINT('',(0.288675134594813,-0.6,0.));
#47703=CARTESIAN_POINT('Origin',(-0.144337567297406,-0.6,-0.25));
#47704=CARTESIAN_POINT('',(-0.144337567297406,-0.6,-0.25));
#47705=CARTESIAN_POINT('',(0.144337567297406,-0.6,-0.25));
#47706=CARTESIAN_POINT('',(-0.144337567297406,-0.96,-0.25));
#47707=CARTESIAN_POINT('',(-0.144337567297406,-0.6,-0.25));
#47708=CARTESIAN_POINT('',(0.144337567297406,-0.96,-0.25));
#47709=CARTESIAN_POINT('Origin',(-0.288675134594813,-0.6,-8.32667268468867E-17));
#47710=CARTESIAN_POINT('',(-0.288675134594813,-0.6,-3.53525079574969E-17));
#47711=CARTESIAN_POINT('',(-0.144337567297406,-0.6,-0.25));
#47712=CARTESIAN_POINT('',(-0.288675134594813,-0.96,-5.55111512312578E-17));
#47713=CARTESIAN_POINT('',(-0.288675134594813,-0.6,-3.53525079574969E-17));
#47714=CARTESIAN_POINT('',(-0.144337567297406,-0.96,-0.25));
#47715=CARTESIAN_POINT('Origin',(-0.144337567297407,-0.6,0.25));
#47716=CARTESIAN_POINT('',(-0.144337567297407,-0.6,0.25));
#47717=CARTESIAN_POINT('',(-0.288675134594813,-0.6,-3.53525079574969E-17));
#47718=CARTESIAN_POINT('',(-0.144337567297407,-0.96,0.25));
#47719=CARTESIAN_POINT('',(-0.144337567297407,-0.6,0.25));
#47720=CARTESIAN_POINT('',(-0.288675134594813,-0.96,-3.53525079574969E-17));
#47721=CARTESIAN_POINT('Origin',(0.144337567297406,-0.6,0.25));
#47722=CARTESIAN_POINT('',(0.144337567297406,-0.6,0.25));
#47723=CARTESIAN_POINT('',(-0.144337567297407,-0.6,0.25));
#47724=CARTESIAN_POINT('',(0.144337567297406,-0.96,0.25));
#47725=CARTESIAN_POINT('',(0.144337567297406,-0.6,0.25));
#47726=CARTESIAN_POINT('',(-0.144337567297407,-0.96,0.25));
#47727=CARTESIAN_POINT('Origin',(0.288675134594813,-0.6,0.));
#47728=CARTESIAN_POINT('',(0.144337567297406,-0.6,0.25));
#47729=CARTESIAN_POINT('',(0.144337567297406,-0.96,0.25));
#47730=CARTESIAN_POINT('Origin',(0.,-0.6,0.));
#47731=CARTESIAN_POINT('Origin',(0.,-0.96,0.));
#62836=UNCERTAINTY_MEASURE_WITH_UNIT(LENGTH_MEASURE(0.001),#62985,
'DISTANCE_ACCURACY_VALUE',
'Maximum model space distance between geometric entities at asserted c
onnectivities');
#62885=UNCERTAINTY_MEASURE_WITH_UNIT(LENGTH_MEASURE(0.001),#62985,
'DISTANCE_ACCURACY_VALUE',
'Maximum model space distance between geometric entities at asserted c
onnectivities');
#62935=(
GEOMETRIC_REPRESENTATION_CONTEXT(3)
GLOBAL_UNCERTAINTY_ASSIGNED_CONTEXT((#62836))
GLOBAL_UNIT_ASSIGNED_CONTEXT((#62985,#62987,#62988))
REPRESENTATION_CONTEXT('','3D')
);
#62984=(
GEOMETRIC_REPRESENTATION_CONTEXT(3)
GLOBAL_UNCERTAINTY_ASSIGNED_CONTEXT((#62885))
GLOBAL_UNIT_ASSIGNED_CONTEXT((#62985,#62987,#62988))
REPRESENTATION_CONTEXT('','3D')
);
#62985=(
LENGTH_UNIT()
NAMED_UNIT(*)
SI_UNIT(.CENTI.,.METRE.)
);
#62987=(
NAMED_UNIT(*)
PLANE_ANGLE_UNIT()
SI_UNIT($,.RADIAN.)
);
#62988=(
NAMED_UNIT(*)
SI_UNIT($,.STERADIAN.)
SOLID_ANGLE_UNIT()
);
#63038=SHAPE_DEFINITION_REPRESENTATION(#63169,#63398);
#63169=PRODUCT_DEFINITION_SHAPE('',$,#63497);
#63398=SHAPE_REPRESENTATION('',(#25127),#62935);
#63447=PRODUCT_DEFINITION_CONTEXT('part definition',#63743,'design');
#63497=PRODUCT_DEFINITION('Cap Screw - M6x25','Cap Screw - M6x25',#63595,
#63447);
#63595=PRODUCT_DEFINITION_FORMATION('',$,#63794);
#63743=APPLICATION_CONTEXT(
'Core Data for Automotive Mechanical Design Process');
#63744=PRODUCT_CONTEXT('part definition',#63743,'mechanical');
#63794=PRODUCT('Cap Screw - M6x25','Cap Screw - M6x25',
'Cap Screw - M6x25',(#63744));
#63913=COLOUR_RGB('Black',0.12,0.14,0.17);
#63914=FILL_AREA_STYLE_COLOUR('',#63913);
#63915=FILL_AREA_STYLE('',(#63914));
#63916=SURFACE_STYLE_FILL_AREA(#63915);
#63917=SURFACE_SIDE_STYLE('',(#63916));
#63918=SURFACE_STYLE_USAGE(.BOTH.,#63917);
#63919=PRESENTATION_STYLE_ASSIGNMENT((#63918));
ENDSEC;
END-ISO-10303-21;
